ISO-10303-21;
HEADER;
/* Generated by software containing ST-Developer
 * from STEP Tools, Inc. (www.steptools.com) 
 */
/* OPTION: using custom renumber hook */

FILE_DESCRIPTION(
/* description */ ('STEP AP242 Edition 2', 'CAx-IF Rec.Pracs.---Representation and Presentation of Product Manufa
cturing Information (PMI)---4.0---2014-10-13', 'CAx-IF Rec.Pracs.---3D Tessellated Geometry---0.4---2014-09-14', '2;1', 'CAx-IF Rec.Pracs.---User Defined Attributes---1.5---2016-08-15'),
/* implementation_level */ '2;1');

FILE_NAME(
/* name */ 'Part 3.step',
/* time_stamp */ '2026-10-07T00:00:55Z',
/* author */ (''),
/* organization */ (''),
/* preprocessor_version */ 'ST-DEVELOPER v20',
/* originating_system */ 'ONSHAPE BY PTC INC, 1.221',
/* authorisation */ '  ');

FILE_SCHEMA (('AP242_MANAGED_MODEL_BASED_3D_ENGINEERING_MIM_LF { 1 0 10303 442 3 1 4 }'));
ENDSEC;

DATA;
#127=SHAPE_REPRESENTATION_RELATIONSHIP('','',#4483,#138);
#138=ADVANCED_BREP_SHAPE_REPRESENTATION('',(#4459),#8546);
#306=CYLINDRICAL_SURFACE('',#5055,0.023);
#307=CYLINDRICAL_SURFACE('',#5057,0.024);
#579=CIRCLE('',#5053,0.024);
#580=CIRCLE('',#5054,0.023);
#581=CIRCLE('',#5056,0.023);
#582=CIRCLE('',#5058,0.024);
#1845=ORIENTED_EDGE('',*,*,#2442,.F.);
#1846=ORIENTED_EDGE('',*,*,#2443,.T.);
#1847=ORIENTED_EDGE('',*,*,#2444,.F.);
#1848=ORIENTED_EDGE('',*,*,#2445,.F.);
#1849=ORIENTED_EDGE('',*,*,#2446,.F.);
#1850=ORIENTED_EDGE('',*,*,#2447,.T.);
#1851=ORIENTED_EDGE('',*,*,#2448,.F.);
#1852=ORIENTED_EDGE('',*,*,#2445,.T.);
#1853=ORIENTED_EDGE('',*,*,#2449,.F.);
#1854=ORIENTED_EDGE('',*,*,#2450,.T.);
#1855=ORIENTED_EDGE('',*,*,#2443,.F.);
#1856=ORIENTED_EDGE('',*,*,#2451,.T.);
#1857=ORIENTED_EDGE('',*,*,#2452,.F.);
#1858=ORIENTED_EDGE('',*,*,#2449,.T.);
#1859=ORIENTED_EDGE('',*,*,#2453,.F.);
#1860=ORIENTED_EDGE('',*,*,#2447,.F.);
#1861=ORIENTED_EDGE('',*,*,#2448,.T.);
#1862=ORIENTED_EDGE('',*,*,#2453,.T.);
#1863=ORIENTED_EDGE('',*,*,#2451,.F.);
#1864=ORIENTED_EDGE('',*,*,#2442,.T.);
#1865=ORIENTED_EDGE('',*,*,#2446,.T.);
#1866=ORIENTED_EDGE('',*,*,#2444,.T.);
#1867=ORIENTED_EDGE('',*,*,#2450,.F.);
#1868=ORIENTED_EDGE('',*,*,#2452,.T.);
#2442=EDGE_CURVE('',#2826,#2827,#3004,.T.);
#2443=EDGE_CURVE('',#2826,#2828,#579,.T.);
#2444=EDGE_CURVE('',#2829,#2828,#3005,.T.);
#2445=EDGE_CURVE('',#2827,#2829,#580,.T.);
#2446=EDGE_CURVE('',#2830,#2829,#3006,.T.);
#2447=EDGE_CURVE('',#2830,#2831,#581,.T.);
#2448=EDGE_CURVE('',#2827,#2831,#3007,.F.);
#2449=EDGE_CURVE('',#2832,#2833,#582,.T.);
#2450=EDGE_CURVE('',#2832,#2828,#3008,.T.);
#2451=EDGE_CURVE('',#2826,#2833,#3009,.F.);
#2452=EDGE_CURVE('',#2832,#2830,#3010,.T.);
#2453=EDGE_CURVE('',#2831,#2833,#3011,.T.);
#2826=VERTEX_POINT('',#8508);
#2827=VERTEX_POINT('',#8509);
#2828=VERTEX_POINT('',#8511);
#2829=VERTEX_POINT('',#8513);
#2830=VERTEX_POINT('',#8517);
#2831=VERTEX_POINT('',#8519);
#2832=VERTEX_POINT('',#8523);
#2833=VERTEX_POINT('',#8524);
#3004=LINE('',#8507,#3182);
#3005=LINE('',#8512,#3183);
#3006=LINE('',#8516,#3184);
#3007=LINE('',#8520,#3185);
#3008=LINE('',#8525,#3186);
#3009=LINE('',#8526,#3187);
#3010=LINE('',#8528,#3188);
#3011=LINE('',#8529,#3189);
#3182=VECTOR('',#6372,1.);
#3183=VECTOR('',#6375,1.);
#3184=VECTOR('',#6380,1.);
#3185=VECTOR('',#6383,1.);
#3186=VECTOR('',#6388,1.);
#3187=VECTOR('',#6389,1.);
#3188=VECTOR('',#6392,1.);
#3189=VECTOR('',#6393,1.);
#3561=EDGE_LOOP('',(#1845,#1846,#1847,#1848));
#3562=EDGE_LOOP('',(#1849,#1850,#1851,#1852));
#3563=EDGE_LOOP('',(#1853,#1854,#1855,#1856));
#3564=EDGE_LOOP('',(#1857,#1858,#1859,#1860));
#3565=EDGE_LOOP('',(#1861,#1862,#1863,#1864));
#3566=EDGE_LOOP('',(#1865,#1866,#1867,#1868));
#3938=FACE_BOUND('',#3561,.T.);
#3939=FACE_BOUND('',#3562,.T.);
#3940=FACE_BOUND('',#3563,.T.);
#3941=FACE_BOUND('',#3564,.T.);
#3942=FACE_BOUND('',#3565,.T.);
#3943=FACE_BOUND('',#3566,.T.);
#4032=PLANE('',#5052);
#4033=PLANE('',#5059);
#4034=PLANE('',#5060);
#4035=PLANE('',#5061);
#4317=ADVANCED_FACE('',(#3938),#4032,.T.);
#4318=ADVANCED_FACE('',(#3939),#306,.F.);
#4319=ADVANCED_FACE('',(#3940),#307,.T.);
#4320=ADVANCED_FACE('',(#3941),#4033,.T.);
#4321=ADVANCED_FACE('',(#3942),#4034,.F.);
#4322=ADVANCED_FACE('',(#3943),#4035,.F.);
#4333=CLOSED_SHELL('',(#4317,#4318,#4319,#4320,#4321,#4322));
#4344=STYLED_ITEM('',(#4360),#4459);
#4360=PRESENTATION_STYLE_ASSIGNMENT((#4376));
#4376=SURFACE_STYLE_USAGE(.BOTH.,#4392);
#4392=SURFACE_SIDE_STYLE('',(#4408));
#4408=SURFACE_STYLE_FILL_AREA(#4424);
#4424=FILL_AREA_STYLE('',(#4440));
#4440=FILL_AREA_STYLE_COLOUR('',#4445);
#4445=COLOUR_RGB('', 0.31764706, 0.68627451, 0.89019608);
#4459=MANIFOLD_SOLID_BREP('Part 3',#4333);
#4471=SHAPE_DEFINITION_REPRESENTATION(#8586,#4483);
#4483=SHAPE_REPRESENTATION('Part 3',(#4484),#8546);
#4484=AXIS2_PLACEMENT_3D('',#6402,#5064,#5065);
#5052=AXIS2_PLACEMENT_3D('',#8506,#6370,#6371);
#5053=AXIS2_PLACEMENT_3D('',#8510,#6373,#6374);
#5054=AXIS2_PLACEMENT_3D('',#8514,#6376,#6377);
#5055=AXIS2_PLACEMENT_3D('',#8515,#6378,#6379);
#5056=AXIS2_PLACEMENT_3D('',#8518,#6381,#6382);
#5057=AXIS2_PLACEMENT_3D('',#8521,#6384,#6385);
#5058=AXIS2_PLACEMENT_3D('',#8522,#6386,#6387);
#5059=AXIS2_PLACEMENT_3D('',#8527,#6390,#6391);
#5060=AXIS2_PLACEMENT_3D('',#8530,#6394,#6395);
#5061=AXIS2_PLACEMENT_3D('',#8531,#6396,#6397);
#5064=DIRECTION('',(0.,0.,1.));
#5065=DIRECTION('',(1.,0.,0.));
#6370=DIRECTION('',(0.,0.,-1.));
#6371=DIRECTION('',(1.,0.,0.));
#6372=DIRECTION('',(-1.,0.,0.));
#6373=DIRECTION('',(0.,0.,-1.));
#6374=DIRECTION('',(-1.,0.,0.));
#6375=DIRECTION('',(-1.,0.,0.));
#6376=DIRECTION('',(0.,0.,-1.));
#6377=DIRECTION('',(-1.,0.,0.));
#6378=DIRECTION('',(0.,0.,-1.));
#6379=DIRECTION('',(-1.,0.,0.));
#6380=DIRECTION('',(0.,0.,-1.));
#6381=DIRECTION('',(0.,0.,1.));
#6382=DIRECTION('',(1.,0.,0.));
#6383=DIRECTION('',(0.,0.,-1.));
#6384=DIRECTION('',(0.,0.,-1.));
#6385=DIRECTION('',(-1.,0.,0.));
#6386=DIRECTION('',(0.,0.,1.));
#6387=DIRECTION('',(1.,0.,0.));
#6388=DIRECTION('',(0.,0.,-1.));
#6389=DIRECTION('',(0.,0.,-1.));
#6390=DIRECTION('',(0.,0.,1.));
#6391=DIRECTION('',(1.,0.,0.));
#6392=DIRECTION('',(1.,0.,0.));
#6393=DIRECTION('',(1.,0.,0.));
#6394=DIRECTION('',(0.,-1.,0.));
#6395=DIRECTION('',(1.,0.,0.));
#6396=DIRECTION('',(0.,-1.,0.));
#6397=DIRECTION('',(1.,0.,0.));
#6402=CARTESIAN_POINT('',(0.,0.,0.));
#8506=CARTESIAN_POINT('',(0.,0.,-0.0130000004));
#8507=CARTESIAN_POINT('',(0.,-0.0746532949430514,-0.0130000004));
#8508=CARTESIAN_POINT('',(0.0231769772486856,-0.0746532949430514,-0.0130000004));
#8509=CARTESIAN_POINT('',(0.0221398345609468,-0.0746532949430514,-0.0130000004));
#8510=CARTESIAN_POINT('',(-1.7347234759768E-18,-0.0684221052,-0.0130000004));
#8511=CARTESIAN_POINT('',(-0.0231769772486856,-0.0746532949430514,-0.0130000004));
#8512=CARTESIAN_POINT('',(0.,-0.0746532949430514,-0.0130000004));
#8513=CARTESIAN_POINT('',(-0.0221398345609468,-0.0746532949430514,-0.0130000004));
#8514=CARTESIAN_POINT('',(-5.08934448853094E-19,-0.0684221052,-0.0130000004));
#8515=CARTESIAN_POINT('',(-5.08934448853094E-19,-0.0684221052,0.0130020004));
#8516=CARTESIAN_POINT('',(-0.0221398345609468,-0.0746532949430514,0.0130020004));
#8517=CARTESIAN_POINT('',(-0.0221398345609468,-0.0746532949430514,0.0130000004));
#8518=CARTESIAN_POINT('',(-5.08934448853094E-19,-0.0684221052,0.0130000004));
#8519=CARTESIAN_POINT('',(0.0221398345609468,-0.0746532949430514,0.0130000004));
#8520=CARTESIAN_POINT('',(0.0221398345609468,-0.0746532949430514,0.0130020004));
#8521=CARTESIAN_POINT('',(-1.7347234759768E-18,-0.0684221052,0.0130020004));
#8522=CARTESIAN_POINT('',(-1.7347234759768E-18,-0.0684221052,0.0130000004));
#8523=CARTESIAN_POINT('',(-0.0231769772486856,-0.0746532949430514,0.0130000004));
#8524=CARTESIAN_POINT('',(0.0231769772486856,-0.0746532949430514,0.0130000004));
#8525=CARTESIAN_POINT('',(-0.0231769772486856,-0.0746532949430514,0.0130020004));
#8526=CARTESIAN_POINT('',(0.0231769772486856,-0.0746532949430514,0.0130020004));
#8527=CARTESIAN_POINT('',(0.,0.,0.0130000004));
#8528=CARTESIAN_POINT('',(0.,-0.0746532949430514,0.0130000004));
#8529=CARTESIAN_POINT('',(0.,-0.0746532949430514,0.0130000004));
#8530=CARTESIAN_POINT('',(0.0434268042445183,-0.0746532949430514,0.0110000004));
#8531=CARTESIAN_POINT('',(0.0434268042445183,-0.0746532949430514,0.0110000004));
#8534=MECHANICAL_DESIGN_GEOMETRIC_PRESENTATION_REPRESENTATION('',(#4344),#8535);
#8535=(
GEOMETRIC_REPRESENTATION_CONTEXT(3)
GLOBAL_UNCERTAINTY_ASSIGNED_CONTEXT((#8547))
GLOBAL_UNIT_ASSIGNED_CONTEXT((#8561,#8560,#8559))
REPRESENTATION_CONTEXT('MAS-680','TOP_LEVEL_ASSEMBLY_PART')
);
#8546=(
GEOMETRIC_REPRESENTATION_CONTEXT(3)
GLOBAL_UNCERTAINTY_ASSIGNED_CONTEXT((#8558))
GLOBAL_UNIT_ASSIGNED_CONTEXT((#8561,#8560,#8559))
REPRESENTATION_CONTEXT('Part 3','COMPONENT_PART')
);
#8547=UNCERTAINTY_MEASURE_WITH_UNIT(LENGTH_MEASURE(1.E-8),#8561,
'DISTANCE_ACCURACY_VALUE','Maximum Tolerance applied to model');
#8558=UNCERTAINTY_MEASURE_WITH_UNIT(LENGTH_MEASURE(1.E-8),#8561,
'DISTANCE_ACCURACY_VALUE','Maximum Tolerance applied to model');
#8559=(
NAMED_UNIT(*)
SI_UNIT($,.STERADIAN.)
SOLID_ANGLE_UNIT()
);
#8560=(
NAMED_UNIT(*)
PLANE_ANGLE_UNIT()
SI_UNIT($,.RADIAN.)
);
#8561=(
LENGTH_UNIT()
NAMED_UNIT(*)
SI_UNIT($,.METRE.)
);
#8586=PRODUCT_DEFINITION_SHAPE('','',#8600);
#8600=PRODUCT_DEFINITION('','',#8624,#8612);
#8612=PRODUCT_DEFINITION_CONTEXT('',#8674,'design');
#8624=PRODUCT_DEFINITION_FORMATION_WITH_SPECIFIED_SOURCE('','',#8648,
 .NOT_KNOWN.);
#8648=PRODUCT('Part 3','Part 3','Part 3',(#8672));
#8672=PRODUCT_CONTEXT('',#8674,'mechanical');
#8674=APPLICATION_CONTEXT('managed model based 3d engineering');
ENDSEC;
END-ISO-10303-21;
